ISO-10303-21;
HEADER;
/* Generated by software containing ST-Developer
 * from STEP Tools, Inc. (www.steptools.com) 
 */

FILE_DESCRIPTION(
/* description */ ('Gravity roller conveyor section'),
/* implementation_level */ '2;1');

FILE_NAME(
/* name */ 'Axle keeper (1).step',
/* time_stamp */ '2026-11-02T07:43:02-08:00',
/* author */ (''),
/* organization */ (''),
/* preprocessor_version */ 'ST-DEVELOPER v20.2',
/* originating_system */ 'Autodesk Translation Framework v15.17.0.0',
/* authorisation */ '');

FILE_SCHEMA (('AUTOMOTIVE_DESIGN { 1 0 10303 214 3 1 1 }'));
ENDSEC;

DATA;
#10=MECHANICAL_DESIGN_GEOMETRIC_PRESENTATION_REPRESENTATION('',(#567),#13821);
#491=SHAPE_REPRESENTATION_RELATIONSHIP('SRR','None',#14030,#525);
#525=ADVANCED_BREP_SHAPE_REPRESENTATION('',(#606),#13817);
#567=STYLED_ITEM('',(#14192),#606);
#606=MANIFOLD_SOLID_BREP('Body1',#7668);
#690=FACE_BOUND('',#1882,.T.);
#691=FACE_BOUND('',#1884,.T.);
#973=PLANE('',#8657);
#974=PLANE('',#8658);
#1379=FACE_OUTER_BOUND('',#1879,.T.);
#1380=FACE_OUTER_BOUND('',#1880,.T.);
#1381=FACE_OUTER_BOUND('',#1881,.T.);
#1382=FACE_OUTER_BOUND('',#1883,.T.);
#1879=EDGE_LOOP('',(#6926,#6927,#6928,#6929));
#1880=EDGE_LOOP('',(#6930,#6931,#6932,#6933));
#1881=EDGE_LOOP('',(#6934));
#1882=EDGE_LOOP('',(#6935));
#1883=EDGE_LOOP('',(#6936));
#1884=EDGE_LOOP('',(#6937));
#2581=LINE('',#13440,#3299);
#2582=LINE('',#13446,#3300);
#3299=VECTOR('',#10670,0.225);
#3300=VECTOR('',#10677,0.7);
#3565=CIRCLE('',#8652,0.225);
#3566=CIRCLE('',#8653,0.225);
#3567=CIRCLE('',#8655,0.7);
#3568=CIRCLE('',#8656,0.7);
#4171=VERTEX_POINT('',#13437);
#4172=VERTEX_POINT('',#13439);
#4173=VERTEX_POINT('',#13443);
#4174=VERTEX_POINT('',#13445);
#5100=EDGE_CURVE('',#4171,#4171,#3565,.T.);
#5101=EDGE_CURVE('',#4171,#4172,#2581,.T.);
#5102=EDGE_CURVE('',#4172,#4172,#3566,.T.);
#5103=EDGE_CURVE('',#4173,#4173,#3567,.T.);
#5104=EDGE_CURVE('',#4173,#4174,#2582,.T.);
#5105=EDGE_CURVE('',#4174,#4174,#3568,.T.);
#6926=ORIENTED_EDGE('',*,*,#5100,.F.);
#6927=ORIENTED_EDGE('',*,*,#5101,.T.);
#6928=ORIENTED_EDGE('',*,*,#5102,.T.);
#6929=ORIENTED_EDGE('',*,*,#5101,.F.);
#6930=ORIENTED_EDGE('',*,*,#5103,.F.);
#6931=ORIENTED_EDGE('',*,*,#5104,.T.);
#6932=ORIENTED_EDGE('',*,*,#5105,.T.);
#6933=ORIENTED_EDGE('',*,*,#5104,.F.);
#6934=ORIENTED_EDGE('',*,*,#5103,.T.);
#6935=ORIENTED_EDGE('',*,*,#5100,.T.);
#6936=ORIENTED_EDGE('',*,*,#5105,.F.);
#6937=ORIENTED_EDGE('',*,*,#5102,.F.);
#7198=CYLINDRICAL_SURFACE('',#8651,0.225);
#7199=CYLINDRICAL_SURFACE('',#8654,0.7);
#7580=ADVANCED_FACE('',(#1379),#7198,.F.);
#7581=ADVANCED_FACE('',(#1380),#7199,.T.);
#7582=ADVANCED_FACE('',(#1381,#690),#973,.T.);
#7583=ADVANCED_FACE('',(#1382,#691),#974,.F.);
#7668=CLOSED_SHELL('',(#7580,#7581,#7582,#7583));
#8650=AXIS2_PLACEMENT_3D('',#13435,#10664,#10665);
#8651=AXIS2_PLACEMENT_3D('',#13436,#10666,#10667);
#8652=AXIS2_PLACEMENT_3D('',#13438,#10668,#10669);
#8653=AXIS2_PLACEMENT_3D('',#13441,#10671,#10672);
#8654=AXIS2_PLACEMENT_3D('',#13442,#10673,#10674);
#8655=AXIS2_PLACEMENT_3D('',#13444,#10675,#10676);
#8656=AXIS2_PLACEMENT_3D('',#13447,#10678,#10679);
#8657=AXIS2_PLACEMENT_3D('',#13448,#10680,#10681);
#8658=AXIS2_PLACEMENT_3D('',#13449,#10682,#10683);
#10664=DIRECTION('axis',(0.,0.,1.));
#10665=DIRECTION('refdir',(1.,0.,0.));
#10666=DIRECTION('center_axis',(0.,1.,0.));
#10667=DIRECTION('ref_axis',(1.,0.,0.));
#10668=DIRECTION('center_axis',(0.,-1.,0.));
#10669=DIRECTION('ref_axis',(1.,0.,0.));
#10670=DIRECTION('',(0.,-1.,0.));
#10671=DIRECTION('center_axis',(0.,-1.,0.));
#10672=DIRECTION('ref_axis',(1.,0.,0.));
#10673=DIRECTION('center_axis',(0.,1.,0.));
#10674=DIRECTION('ref_axis',(1.,0.,0.));
#10675=DIRECTION('center_axis',(0.,1.,0.));
#10676=DIRECTION('ref_axis',(1.,0.,0.));
#10677=DIRECTION('',(0.,-1.,0.));
#10678=DIRECTION('center_axis',(0.,1.,0.));
#10679=DIRECTION('ref_axis',(1.,0.,0.));
#10680=DIRECTION('center_axis',(0.,1.,0.));
#10681=DIRECTION('ref_axis',(1.,0.,0.));
#10682=DIRECTION('center_axis',(0.,1.,0.));
#10683=DIRECTION('ref_axis',(1.,0.,0.));
#13435=CARTESIAN_POINT('',(0.,0.,0.));
#13436=CARTESIAN_POINT('Origin',(3.,33.,8.));
#13437=CARTESIAN_POINT('',(2.775,33.2,8.));
#13438=CARTESIAN_POINT('Origin',(3.,33.2,8.));
#13439=CARTESIAN_POINT('',(2.775,33.,8.));
#13440=CARTESIAN_POINT('',(2.775,33.,8.));
#13441=CARTESIAN_POINT('Origin',(3.,33.,8.));
#13442=CARTESIAN_POINT('Origin',(3.,33.,8.));
#13443=CARTESIAN_POINT('',(2.3,33.2,8.));
#13444=CARTESIAN_POINT('Origin',(3.,33.2,8.));
#13445=CARTESIAN_POINT('',(2.3,33.,8.));
#13446=CARTESIAN_POINT('',(2.3,33.,8.));
#13447=CARTESIAN_POINT('Origin',(3.,33.,8.));
#13448=CARTESIAN_POINT('Origin',(3.,33.2,8.));
#13449=CARTESIAN_POINT('Origin',(3.,33.,8.));
#13778=UNCERTAINTY_MEASURE_WITH_UNIT(LENGTH_MEASURE(0.001),#13822,
'DISTANCE_ACCURACY_VALUE',
'Maximum model space distance between geometric entities at asserted c
onnectivities');
#13782=UNCERTAINTY_MEASURE_WITH_UNIT(LENGTH_MEASURE(0.001),#13822,
'DISTANCE_ACCURACY_VALUE',
'Maximum model space distance between geometric entities at asserted c
onnectivities');
#13817=(
GEOMETRIC_REPRESENTATION_CONTEXT(3)
GLOBAL_UNCERTAINTY_ASSIGNED_CONTEXT((#13778))
GLOBAL_UNIT_ASSIGNED_CONTEXT((#13822,#13824,#13825))
REPRESENTATION_CONTEXT('','3D')
);
#13821=(
GEOMETRIC_REPRESENTATION_CONTEXT(3)
GLOBAL_UNCERTAINTY_ASSIGNED_CONTEXT((#13782))
GLOBAL_UNIT_ASSIGNED_CONTEXT((#13822,#13824,#13825))
REPRESENTATION_CONTEXT('','3D')
);
#13822=(
LENGTH_UNIT()
NAMED_UNIT(*)
SI_UNIT(.CENTI.,.METRE.)
);
#13824=(
NAMED_UNIT(*)
PLANE_ANGLE_UNIT()
SI_UNIT($,.RADIAN.)
);
#13825=(
NAMED_UNIT(*)
SI_UNIT($,.STERADIAN.)
SOLID_ANGLE_UNIT()
);
#13860=SHAPE_DEFINITION_REPRESENTATION(#13903,#14030);
#13903=PRODUCT_DEFINITION_SHAPE('',$,#14069);
#14030=SHAPE_REPRESENTATION('',(#8650),#13817);
#14034=PRODUCT_DEFINITION_CONTEXT('part definition',#14150,'design');
#14069=PRODUCT_DEFINITION('Axle keeper_1','Axle keeper (1)',#14107,#14034);
#14107=PRODUCT_DEFINITION_FORMATION('',$,#14186);
#14150=APPLICATION_CONTEXT(
'Core Data for Automotive Mechanical Design Process');
#14151=PRODUCT_CONTEXT('part definition',#14150,'mechanical');
#14186=PRODUCT('Axle keeper_1','Axle keeper (1)','Axle keeper',(#14151));
#14192=PRESENTATION_STYLE_ASSIGNMENT((#14197));
#14197=SURFACE_STYLE_USAGE(.BOTH.,#14202);
#14202=SURFACE_SIDE_STYLE('',(#14207));
#14207=SURFACE_STYLE_FILL_AREA(#14212);
#14212=FILL_AREA_STYLE('CAD Library Painted - Engineering blue',(#14217));
#14217=FILL_AREA_STYLE_COLOUR('CAD Library Painted - Engineering blue',
#14222);
#14222=COLOUR_RGB('CAD Library Painted - Engineering blue',0.12156862745098,
0.356862745098039,0.6);
ENDSEC;
END-ISO-10303-21;
